ISO-10303-21;
HEADER;
/* Generated by software containing ST-Developer
 * from STEP Tools, Inc. (www.steptools.com) 
 */

FILE_DESCRIPTION(
/* description */ ('PAT-091'),
/* implementation_level */ '2;1');

FILE_NAME(
/* name */ 'Linear bearing keeper (2).step',
/* time_stamp */ '2026-10-27T15:34:44-07:00',
/* author */ (''),
/* organization */ (''),
/* preprocessor_version */ 'ST-DEVELOPER v20.2',
/* originating_system */ 'Autodesk Translation Framework v15.17.0.0',
/* authorisation */ '');

FILE_SCHEMA (('AUTOMOTIVE_DESIGN { 1 0 10303 214 3 1 1 }'));
ENDSEC;

DATA;
#10=MECHANICAL_DESIGN_GEOMETRIC_PRESENTATION_REPRESENTATION('',(#1014),#25100);
#794=SHAPE_REPRESENTATION_RELATIONSHIP('SRR','None',#25558,#904);
#904=ADVANCED_BREP_SHAPE_REPRESENTATION('',(#1136),#25028);
#1014=STYLED_ITEM('',(#26191),#1136);
#1136=MANIFOLD_SOLID_BREP('Body1',#13293);
#1438=FACE_BOUND('',#3451,.T.);
#1439=FACE_BOUND('',#3454,.T.);
#1440=FACE_BOUND('',#3463,.T.);
#1441=FACE_BOUND('',#3464,.T.);
#1442=FACE_BOUND('',#3465,.T.);
#1443=FACE_BOUND('',#3467,.T.);
#1444=FACE_BOUND('',#3468,.T.);
#1445=FACE_BOUND('',#3469,.T.);
#1829=PLANE('',#15289);
#1830=PLANE('',#15294);
#1831=PLANE('',#15303);
#1832=PLANE('',#15304);
#1833=PLANE('',#15305);
#1834=PLANE('',#15306);
#1835=PLANE('',#15307);
#1836=PLANE('',#15308);
#2408=FACE_OUTER_BOUND('',#3449,.T.);
#2409=FACE_OUTER_BOUND('',#3450,.T.);
#2410=FACE_OUTER_BOUND('',#3452,.T.);
#2411=FACE_OUTER_BOUND('',#3453,.T.);
#2412=FACE_OUTER_BOUND('',#3455,.T.);
#2413=FACE_OUTER_BOUND('',#3456,.T.);
#2414=FACE_OUTER_BOUND('',#3457,.T.);
#2415=FACE_OUTER_BOUND('',#3458,.T.);
#2416=FACE_OUTER_BOUND('',#3459,.T.);
#2417=FACE_OUTER_BOUND('',#3460,.T.);
#2418=FACE_OUTER_BOUND('',#3461,.T.);
#2419=FACE_OUTER_BOUND('',#3462,.T.);
#2420=FACE_OUTER_BOUND('',#3466,.T.);
#3449=EDGE_LOOP('',(#10386,#10387,#10388,#10389));
#3450=EDGE_LOOP('',(#10390));
#3451=EDGE_LOOP('',(#10391));
#3452=EDGE_LOOP('',(#10392,#10393,#10394,#10395));
#3453=EDGE_LOOP('',(#10396));
#3454=EDGE_LOOP('',(#10397));
#3455=EDGE_LOOP('',(#10398,#10399,#10400,#10401));
#3456=EDGE_LOOP('',(#10402,#10403,#10404,#10405));
#3457=EDGE_LOOP('',(#10406,#10407,#10408,#10409));
#3458=EDGE_LOOP('',(#10410,#10411,#10412,#10413));
#3459=EDGE_LOOP('',(#10414,#10415,#10416,#10417));
#3460=EDGE_LOOP('',(#10418,#10419,#10420,#10421));
#3461=EDGE_LOOP('',(#10422,#10423,#10424,#10425));
#3462=EDGE_LOOP('',(#10426,#10427,#10428,#10429));
#3463=EDGE_LOOP('',(#10430));
#3464=EDGE_LOOP('',(#10431));
#3465=EDGE_LOOP('',(#10432));
#3466=EDGE_LOOP('',(#10433,#10434,#10435,#10436));
#3467=EDGE_LOOP('',(#10437));
#3468=EDGE_LOOP('',(#10438));
#3469=EDGE_LOOP('',(#10439));
#4522=LINE('',#22574,#5262);
#4523=LINE('',#22583,#5263);
#4524=LINE('',#22592,#5264);
#4525=LINE('',#22597,#5265);
#4526=LINE('',#22601,#5266);
#4527=LINE('',#22605,#5267);
#4528=LINE('',#22607,#5268);
#4529=LINE('',#22609,#5269);
#4530=LINE('',#22610,#5270);
#4531=LINE('',#22613,#5271);
#4532=LINE('',#22615,#5272);
#4533=LINE('',#22616,#5273);
#4534=LINE('',#22619,#5274);
#4535=LINE('',#22621,#5275);
#4536=LINE('',#22622,#5276);
#4537=LINE('',#22624,#5277);
#4538=LINE('',#22625,#5278);
#5262=VECTOR('',#18272,1.04);
#5263=VECTOR('',#18283,1.04);
#5264=VECTOR('',#18294,0.65);
#5265=VECTOR('',#18301,0.800000000000001);
#5266=VECTOR('',#18306,0.800000000000001);
#5267=VECTOR('',#18309,1.);
#5268=VECTOR('',#18310,1.);
#5269=VECTOR('',#18311,1.);
#5270=VECTOR('',#18312,1.);
#5271=VECTOR('',#18315,1.);
#5272=VECTOR('',#18316,1.);
#5273=VECTOR('',#18317,1.);
#5274=VECTOR('',#18320,1.);
#5275=VECTOR('',#18321,1.);
#5276=VECTOR('',#18322,1.);
#5277=VECTOR('',#18325,1.);
#5278=VECTOR('',#18326,1.);
#5911=CIRCLE('',#15287,1.04);
#5912=CIRCLE('',#15288,1.04);
#5913=CIRCLE('',#15290,0.800000000000001);
#5914=CIRCLE('',#15292,1.04);
#5915=CIRCLE('',#15293,1.04);
#5916=CIRCLE('',#15295,0.800000000000001);
#5917=CIRCLE('',#15297,0.65);
#5918=CIRCLE('',#15298,0.65);
#5919=CIRCLE('',#15300,0.800000000000001);
#5920=CIRCLE('',#15302,0.800000000000001);
#6852=VERTEX_POINT('',#22571);
#6853=VERTEX_POINT('',#22573);
#6854=VERTEX_POINT('',#22577);
#6855=VERTEX_POINT('',#22580);
#6856=VERTEX_POINT('',#22582);
#6857=VERTEX_POINT('',#22586);
#6858=VERTEX_POINT('',#22589);
#6859=VERTEX_POINT('',#22591);
#6860=VERTEX_POINT('',#22595);
#6861=VERTEX_POINT('',#22599);
#6862=VERTEX_POINT('',#22603);
#6863=VERTEX_POINT('',#22604);
#6864=VERTEX_POINT('',#22606);
#6865=VERTEX_POINT('',#22608);
#6866=VERTEX_POINT('',#22612);
#6867=VERTEX_POINT('',#22614);
#6868=VERTEX_POINT('',#22618);
#6869=VERTEX_POINT('',#22620);
#8128=EDGE_CURVE('',#6852,#6852,#5911,.T.);
#8129=EDGE_CURVE('',#6852,#6853,#4522,.T.);
#8130=EDGE_CURVE('',#6853,#6853,#5912,.T.);
#8131=EDGE_CURVE('',#6854,#6854,#5913,.T.);
#8132=EDGE_CURVE('',#6855,#6855,#5914,.T.);
#8133=EDGE_CURVE('',#6855,#6856,#4523,.T.);
#8134=EDGE_CURVE('',#6856,#6856,#5915,.T.);
#8135=EDGE_CURVE('',#6857,#6857,#5916,.T.);
#8136=EDGE_CURVE('',#6858,#6858,#5917,.T.);
#8137=EDGE_CURVE('',#6858,#6859,#4524,.T.);
#8138=EDGE_CURVE('',#6859,#6859,#5918,.T.);
#8139=EDGE_CURVE('',#6860,#6860,#5919,.T.);
#8140=EDGE_CURVE('',#6860,#6857,#4525,.T.);
#8141=EDGE_CURVE('',#6861,#6861,#5920,.T.);
#8142=EDGE_CURVE('',#6861,#6854,#4526,.T.);
#8143=EDGE_CURVE('',#6862,#6863,#4527,.T.);
#8144=EDGE_CURVE('',#6863,#6864,#4528,.T.);
#8145=EDGE_CURVE('',#6865,#6864,#4529,.T.);
#8146=EDGE_CURVE('',#6862,#6865,#4530,.T.);
#8147=EDGE_CURVE('',#6866,#6862,#4531,.T.);
#8148=EDGE_CURVE('',#6867,#6865,#4532,.T.);
#8149=EDGE_CURVE('',#6866,#6867,#4533,.T.);
#8150=EDGE_CURVE('',#6868,#6866,#4534,.T.);
#8151=EDGE_CURVE('',#6869,#6867,#4535,.T.);
#8152=EDGE_CURVE('',#6868,#6869,#4536,.T.);
#8153=EDGE_CURVE('',#6863,#6868,#4537,.T.);
#8154=EDGE_CURVE('',#6864,#6869,#4538,.T.);
#10386=ORIENTED_EDGE('',*,*,#8128,.F.);
#10387=ORIENTED_EDGE('',*,*,#8129,.T.);
#10388=ORIENTED_EDGE('',*,*,#8130,.F.);
#10389=ORIENTED_EDGE('',*,*,#8129,.F.);
#10390=ORIENTED_EDGE('',*,*,#8128,.T.);
#10391=ORIENTED_EDGE('',*,*,#8131,.T.);
#10392=ORIENTED_EDGE('',*,*,#8132,.F.);
#10393=ORIENTED_EDGE('',*,*,#8133,.T.);
#10394=ORIENTED_EDGE('',*,*,#8134,.F.);
#10395=ORIENTED_EDGE('',*,*,#8133,.F.);
#10396=ORIENTED_EDGE('',*,*,#8132,.T.);
#10397=ORIENTED_EDGE('',*,*,#8135,.T.);
#10398=ORIENTED_EDGE('',*,*,#8136,.F.);
#10399=ORIENTED_EDGE('',*,*,#8137,.T.);
#10400=ORIENTED_EDGE('',*,*,#8138,.F.);
#10401=ORIENTED_EDGE('',*,*,#8137,.F.);
#10402=ORIENTED_EDGE('',*,*,#8139,.F.);
#10403=ORIENTED_EDGE('',*,*,#8140,.T.);
#10404=ORIENTED_EDGE('',*,*,#8135,.F.);
#10405=ORIENTED_EDGE('',*,*,#8140,.F.);
#10406=ORIENTED_EDGE('',*,*,#8141,.F.);
#10407=ORIENTED_EDGE('',*,*,#8142,.T.);
#10408=ORIENTED_EDGE('',*,*,#8131,.F.);
#10409=ORIENTED_EDGE('',*,*,#8142,.F.);
#10410=ORIENTED_EDGE('',*,*,#8143,.T.);
#10411=ORIENTED_EDGE('',*,*,#8144,.T.);
#10412=ORIENTED_EDGE('',*,*,#8145,.F.);
#10413=ORIENTED_EDGE('',*,*,#8146,.F.);
#10414=ORIENTED_EDGE('',*,*,#8147,.T.);
#10415=ORIENTED_EDGE('',*,*,#8146,.T.);
#10416=ORIENTED_EDGE('',*,*,#8148,.F.);
#10417=ORIENTED_EDGE('',*,*,#8149,.F.);
#10418=ORIENTED_EDGE('',*,*,#8150,.T.);
#10419=ORIENTED_EDGE('',*,*,#8149,.T.);
#10420=ORIENTED_EDGE('',*,*,#8151,.F.);
#10421=ORIENTED_EDGE('',*,*,#8152,.F.);
#10422=ORIENTED_EDGE('',*,*,#8153,.T.);
#10423=ORIENTED_EDGE('',*,*,#8152,.T.);
#10424=ORIENTED_EDGE('',*,*,#8154,.F.);
#10425=ORIENTED_EDGE('',*,*,#8144,.F.);
#10426=ORIENTED_EDGE('',*,*,#8154,.T.);
#10427=ORIENTED_EDGE('',*,*,#8151,.T.);
#10428=ORIENTED_EDGE('',*,*,#8148,.T.);
#10429=ORIENTED_EDGE('',*,*,#8145,.T.);
#10430=ORIENTED_EDGE('',*,*,#8130,.T.);
#10431=ORIENTED_EDGE('',*,*,#8134,.T.);
#10432=ORIENTED_EDGE('',*,*,#8138,.T.);
#10433=ORIENTED_EDGE('',*,*,#8153,.F.);
#10434=ORIENTED_EDGE('',*,*,#8143,.F.);
#10435=ORIENTED_EDGE('',*,*,#8147,.F.);
#10436=ORIENTED_EDGE('',*,*,#8150,.F.);
#10437=ORIENTED_EDGE('',*,*,#8136,.T.);
#10438=ORIENTED_EDGE('',*,*,#8139,.T.);
#10439=ORIENTED_EDGE('',*,*,#8141,.T.);
#12223=CYLINDRICAL_SURFACE('',#15286,1.04);
#12224=CYLINDRICAL_SURFACE('',#15291,1.04);
#12225=CYLINDRICAL_SURFACE('',#15296,0.65);
#12226=CYLINDRICAL_SURFACE('',#15299,0.800000000000001);
#12227=CYLINDRICAL_SURFACE('',#15301,0.800000000000001);
#12775=ADVANCED_FACE('',(#2408),#12223,.T.);
#12776=ADVANCED_FACE('',(#2409,#1438),#1829,.T.);
#12777=ADVANCED_FACE('',(#2410),#12224,.T.);
#12778=ADVANCED_FACE('',(#2411,#1439),#1830,.T.);
#12779=ADVANCED_FACE('',(#2412),#12225,.F.);
#12780=ADVANCED_FACE('',(#2413),#12226,.F.);
#12781=ADVANCED_FACE('',(#2414),#12227,.F.);
#12782=ADVANCED_FACE('',(#2415),#1831,.T.);
#12783=ADVANCED_FACE('',(#2416),#1832,.T.);
#12784=ADVANCED_FACE('',(#2417),#1833,.T.);
#12785=ADVANCED_FACE('',(#2418),#1834,.T.);
#12786=ADVANCED_FACE('',(#2419,#1440,#1441,#1442),#1835,.T.);
#12787=ADVANCED_FACE('',(#2420,#1443,#1444,#1445),#1836,.F.);
#13293=CLOSED_SHELL('',(#12775,#12776,#12777,#12778,#12779,#12780,#12781,
#12782,#12783,#12784,#12785,#12786,#12787));
#15285=AXIS2_PLACEMENT_3D('',#22569,#18266,#18267);
#15286=AXIS2_PLACEMENT_3D('',#22570,#18268,#18269);
#15287=AXIS2_PLACEMENT_3D('',#22572,#18270,#18271);
#15288=AXIS2_PLACEMENT_3D('',#22575,#18273,#18274);
#15289=AXIS2_PLACEMENT_3D('',#22576,#18275,#18276);
#15290=AXIS2_PLACEMENT_3D('',#22578,#18277,#18278);
#15291=AXIS2_PLACEMENT_3D('',#22579,#18279,#18280);
#15292=AXIS2_PLACEMENT_3D('',#22581,#18281,#18282);
#15293=AXIS2_PLACEMENT_3D('',#22584,#18284,#18285);
#15294=AXIS2_PLACEMENT_3D('',#22585,#18286,#18287);
#15295=AXIS2_PLACEMENT_3D('',#22587,#18288,#18289);
#15296=AXIS2_PLACEMENT_3D('',#22588,#18290,#18291);
#15297=AXIS2_PLACEMENT_3D('',#22590,#18292,#18293);
#15298=AXIS2_PLACEMENT_3D('',#22593,#18295,#18296);
#15299=AXIS2_PLACEMENT_3D('',#22594,#18297,#18298);
#15300=AXIS2_PLACEMENT_3D('',#22596,#18299,#18300);
#15301=AXIS2_PLACEMENT_3D('',#22598,#18302,#18303);
#15302=AXIS2_PLACEMENT_3D('',#22600,#18304,#18305);
#15303=AXIS2_PLACEMENT_3D('',#22602,#18307,#18308);
#15304=AXIS2_PLACEMENT_3D('',#22611,#18313,#18314);
#15305=AXIS2_PLACEMENT_3D('',#22617,#18318,#18319);
#15306=AXIS2_PLACEMENT_3D('',#22623,#18323,#18324);
#15307=AXIS2_PLACEMENT_3D('',#22626,#18327,#18328);
#15308=AXIS2_PLACEMENT_3D('',#22627,#18329,#18330);
#18266=DIRECTION('axis',(0.,0.,1.));
#18267=DIRECTION('refdir',(1.,0.,0.));
#18268=DIRECTION('center_axis',(1.,0.,0.));
#18269=DIRECTION('ref_axis',(0.,0.,-1.));
#18270=DIRECTION('center_axis',(1.,0.,0.));
#18271=DIRECTION('ref_axis',(0.,0.,-1.));
#18272=DIRECTION('',(-1.,0.,0.));
#18273=DIRECTION('center_axis',(-1.,0.,0.));
#18274=DIRECTION('ref_axis',(0.,0.,-1.));
#18275=DIRECTION('center_axis',(1.,0.,0.));
#18276=DIRECTION('ref_axis',(0.,0.,-1.));
#18277=DIRECTION('center_axis',(-1.,0.,0.));
#18278=DIRECTION('ref_axis',(0.,0.,-1.));
#18279=DIRECTION('center_axis',(1.,0.,0.));
#18280=DIRECTION('ref_axis',(0.,0.,-1.));
#18281=DIRECTION('center_axis',(1.,0.,0.));
#18282=DIRECTION('ref_axis',(0.,0.,-1.));
#18283=DIRECTION('',(-1.,0.,0.));
#18284=DIRECTION('center_axis',(-1.,0.,0.));
#18285=DIRECTION('ref_axis',(0.,0.,-1.));
#18286=DIRECTION('center_axis',(1.,0.,0.));
#18287=DIRECTION('ref_axis',(0.,0.,-1.));
#18288=DIRECTION('center_axis',(-1.,0.,0.));
#18289=DIRECTION('ref_axis',(0.,0.,-1.));
#18290=DIRECTION('center_axis',(1.,0.,0.));
#18291=DIRECTION('ref_axis',(0.,0.,-1.));
#18292=DIRECTION('center_axis',(1.,0.,0.));
#18293=DIRECTION('ref_axis',(0.,0.,-1.));
#18294=DIRECTION('',(1.,0.,0.));
#18295=DIRECTION('center_axis',(-1.,0.,0.));
#18296=DIRECTION('ref_axis',(0.,0.,-1.));
#18297=DIRECTION('center_axis',(1.,0.,0.));
#18298=DIRECTION('ref_axis',(0.,0.,-1.));
#18299=DIRECTION('center_axis',(1.,0.,0.));
#18300=DIRECTION('ref_axis',(0.,0.,-1.));
#18301=DIRECTION('',(1.,0.,0.));
#18302=DIRECTION('center_axis',(1.,0.,0.));
#18303=DIRECTION('ref_axis',(0.,0.,-1.));
#18304=DIRECTION('center_axis',(1.,0.,0.));
#18305=DIRECTION('ref_axis',(0.,0.,-1.));
#18306=DIRECTION('',(1.,0.,0.));
#18307=DIRECTION('center_axis',(0.,0.,1.));
#18308=DIRECTION('ref_axis',(0.,-1.,0.));
#18309=DIRECTION('',(0.,-1.,0.));
#18310=DIRECTION('',(1.,0.,0.));
#18311=DIRECTION('',(0.,-1.,0.));
#18312=DIRECTION('',(1.,0.,0.));
#18313=DIRECTION('center_axis',(0.,1.,0.));
#18314=DIRECTION('ref_axis',(0.,0.,1.));
#18315=DIRECTION('',(0.,0.,1.));
#18316=DIRECTION('',(0.,0.,1.));
#18317=DIRECTION('',(1.,0.,0.));
#18318=DIRECTION('center_axis',(0.,0.,-1.));
#18319=DIRECTION('ref_axis',(0.,1.,0.));
#18320=DIRECTION('',(0.,1.,0.));
#18321=DIRECTION('',(0.,1.,0.));
#18322=DIRECTION('',(1.,0.,0.));
#18323=DIRECTION('center_axis',(0.,-1.,0.));
#18324=DIRECTION('ref_axis',(0.,0.,-1.));
#18325=DIRECTION('',(0.,0.,-1.));
#18326=DIRECTION('',(0.,0.,-1.));
#18327=DIRECTION('center_axis',(1.,0.,0.));
#18328=DIRECTION('ref_axis',(0.,0.,-1.));
#18329=DIRECTION('center_axis',(1.,0.,0.));
#18330=DIRECTION('ref_axis',(0.,0.,-1.));
#22569=CARTESIAN_POINT('',(0.,0.,0.));
#22570=CARTESIAN_POINT('Origin',(37.02983346,3.,16.));
#22571=CARTESIAN_POINT('',(37.22983346,3.,17.04));
#22572=CARTESIAN_POINT('Origin',(37.22983346,3.,16.));
#22573=CARTESIAN_POINT('',(37.02983346,3.,17.04));
#22574=CARTESIAN_POINT('',(37.02983346,3.,17.04));
#22575=CARTESIAN_POINT('Origin',(37.02983346,3.,16.));
#22576=CARTESIAN_POINT('Origin',(37.22983346,3.,16.));
#22577=CARTESIAN_POINT('',(37.22983346,3.,16.8));
#22578=CARTESIAN_POINT('Origin',(37.22983346,3.,16.));
#22579=CARTESIAN_POINT('Origin',(37.02983346,-3.,16.));
#22580=CARTESIAN_POINT('',(37.22983346,-3.,17.04));
#22581=CARTESIAN_POINT('Origin',(37.22983346,-3.,16.));
#22582=CARTESIAN_POINT('',(37.02983346,-3.,17.04));
#22583=CARTESIAN_POINT('',(37.02983346,-3.,17.04));
#22584=CARTESIAN_POINT('Origin',(37.02983346,-3.,16.));
#22585=CARTESIAN_POINT('Origin',(37.22983346,-3.,16.));
#22586=CARTESIAN_POINT('',(37.22983346,-3.,16.8));
#22587=CARTESIAN_POINT('Origin',(37.22983346,-3.,16.));
#22588=CARTESIAN_POINT('Origin',(36.72983346,0.,16.));
#22589=CARTESIAN_POINT('',(36.82983346,-7.9602041944578E-17,16.65));
#22590=CARTESIAN_POINT('Origin',(36.82983346,0.,16.));
#22591=CARTESIAN_POINT('',(37.02983346,7.9602041944578E-17,16.65));
#22592=CARTESIAN_POINT('',(36.72983346,-7.9602041944578E-17,16.65));
#22593=CARTESIAN_POINT('Origin',(37.02983346,0.,16.));
#22594=CARTESIAN_POINT('Origin',(36.72983346,-3.,16.));
#22595=CARTESIAN_POINT('',(36.82983346,-3.,16.8));
#22596=CARTESIAN_POINT('Origin',(36.82983346,-3.,16.));
#22597=CARTESIAN_POINT('',(36.72983346,-3.,16.8));
#22598=CARTESIAN_POINT('Origin',(36.72983346,3.,16.));
#22599=CARTESIAN_POINT('',(36.82983346,3.,16.8));
#22600=CARTESIAN_POINT('Origin',(36.82983346,3.,16.));
#22601=CARTESIAN_POINT('',(36.72983346,3.,16.8));
#22602=CARTESIAN_POINT('Origin',(36.82983346,4.7,17.7));
#22603=CARTESIAN_POINT('',(36.82983346,4.7,17.7));
#22604=CARTESIAN_POINT('',(36.82983346,-4.3,17.7));
#22605=CARTESIAN_POINT('',(36.82983346,4.7,17.7));
#22606=CARTESIAN_POINT('',(37.02983346,-4.3,17.7));
#22607=CARTESIAN_POINT('',(36.82983346,-4.3,17.7));
#22608=CARTESIAN_POINT('',(37.02983346,4.7,17.7));
#22609=CARTESIAN_POINT('',(37.02983346,4.7,17.7));
#22610=CARTESIAN_POINT('',(36.82983346,4.7,17.7));
#22611=CARTESIAN_POINT('Origin',(36.82983346,4.7,14.3));
#22612=CARTESIAN_POINT('',(36.82983346,4.7,14.3));
#22613=CARTESIAN_POINT('',(36.82983346,4.7,14.3));
#22614=CARTESIAN_POINT('',(37.02983346,4.7,14.3));
#22615=CARTESIAN_POINT('',(37.02983346,4.7,14.3));
#22616=CARTESIAN_POINT('',(36.82983346,4.7,14.3));
#22617=CARTESIAN_POINT('Origin',(36.82983346,-4.3,14.3));
#22618=CARTESIAN_POINT('',(36.82983346,-4.3,14.3));
#22619=CARTESIAN_POINT('',(36.82983346,-4.3,14.3));
#22620=CARTESIAN_POINT('',(37.02983346,-4.3,14.3));
#22621=CARTESIAN_POINT('',(37.02983346,-4.3,14.3));
#22622=CARTESIAN_POINT('',(36.82983346,-4.3,14.3));
#22623=CARTESIAN_POINT('Origin',(36.82983346,-4.3,17.7));
#22624=CARTESIAN_POINT('',(36.82983346,-4.3,17.7));
#22625=CARTESIAN_POINT('',(37.02983346,-4.3,17.7));
#22626=CARTESIAN_POINT('Origin',(37.02983346,0.2,16.));
#22627=CARTESIAN_POINT('Origin',(36.82983346,0.2,16.));
#24907=UNCERTAINTY_MEASURE_WITH_UNIT(LENGTH_MEASURE(0.001),#25101,
'DISTANCE_ACCURACY_VALUE',
'Maximum model space distance between geometric entities at asserted c
onnectivities');
#24979=UNCERTAINTY_MEASURE_WITH_UNIT(LENGTH_MEASURE(0.001),#25101,
'DISTANCE_ACCURACY_VALUE',
'Maximum model space distance between geometric entities at asserted c
onnectivities');
#25028=(
GEOMETRIC_REPRESENTATION_CONTEXT(3)
GLOBAL_UNCERTAINTY_ASSIGNED_CONTEXT((#24907))
GLOBAL_UNIT_ASSIGNED_CONTEXT((#25101,#25103,#25104))
REPRESENTATION_CONTEXT('','3D')
);
#25100=(
GEOMETRIC_REPRESENTATION_CONTEXT(3)
GLOBAL_UNCERTAINTY_ASSIGNED_CONTEXT((#24979))
GLOBAL_UNIT_ASSIGNED_CONTEXT((#25101,#25103,#25104))
REPRESENTATION_CONTEXT('','3D')
);
#25101=(
LENGTH_UNIT()
NAMED_UNIT(*)
SI_UNIT(.CENTI.,.METRE.)
);
#25103=(
NAMED_UNIT(*)
PLANE_ANGLE_UNIT()
SI_UNIT($,.RADIAN.)
);
#25104=(
NAMED_UNIT(*)
SI_UNIT($,.STERADIAN.)
SOLID_ANGLE_UNIT()
);
#25153=SHAPE_DEFINITION_REPRESENTATION(#25273,#25558);
#25273=PRODUCT_DEFINITION_SHAPE('',$,#25679);
#25558=SHAPE_REPRESENTATION('',(#15285),#25028);
#25630=PRODUCT_DEFINITION_CONTEXT('part definition',#25992,'design');
#25679=PRODUCT_DEFINITION('Linear bearing keeper (2)',
'Linear bearing keeper (2)',#25799,#25630);
#25799=PRODUCT_DEFINITION_FORMATION('',$,#26042);
#25992=APPLICATION_CONTEXT(
'Core Data for Automotive Mechanical Design Process');
#25993=PRODUCT_CONTEXT('part definition',#25992,'mechanical');
#26042=PRODUCT('Linear bearing keeper (2)','Linear bearing keeper (2)',
'Linear bearing keeper (2)',(#25993));
#26185=COLOUR_RGB('Grey',0.48,0.52,0.57);
#26186=FILL_AREA_STYLE_COLOUR('',#26185);
#26187=FILL_AREA_STYLE('',(#26186));
#26188=SURFACE_STYLE_FILL_AREA(#26187);
#26189=SURFACE_SIDE_STYLE('',(#26188));
#26190=SURFACE_STYLE_USAGE(.BOTH.,#26189);
#26191=PRESENTATION_STYLE_ASSIGNMENT((#26190));
ENDSEC;
END-ISO-10303-21;
